ISO-10303-21;
HEADER;
/* Generated by software containing ST-Developer
 * from STEP Tools, Inc. (www.steptools.com) 
 */

FILE_DESCRIPTION(
/* description */ (''),
/* implementation_level */ '2;1');

FILE_NAME(
/* name */ '19_Air_Inlet_Ball_Valve_1-4.step',
/* time_stamp */ '2026-10-26T06:13:19-07:00',
/* author */ (''),
/* organization */ (''),
/* preprocessor_version */ 'ST-DEVELOPER v20.2',
/* originating_system */ 'Autodesk Translation Framework v15.15.0.0',
/* authorisation */ '');

FILE_SCHEMA (('AUTOMOTIVE_DESIGN { 1 0 10303 214 3 1 1 }','TECHNICAL_DATA_PACKAGING'));
ENDSEC;

DATA;
#10=MECHANICAL_DESIGN_GEOMETRIC_PRESENTATION_REPRESENTATION('',(#308),#56639);
#254=ELLIPSE('',#18087,3.46410161513776,3.);
#255=ELLIPSE('',#18088,3.46410161513776,3.);
#256=ELLIPSE('',#18089,3.46410161513776,3.);
#268=SHAPE_REPRESENTATION_RELATIONSHIP('SRR','None',#56756,#288);
#288=ADVANCED_BREP_SHAPE_REPRESENTATION('',(#328),#56630);
#308=STYLED_ITEM('',(#56929),#328);
#328=MANIFOLD_SOLID_BREP('Body1',#16960);
#536=FACE_BOUND('',#3360,.T.);
#537=FACE_BOUND('',#3383,.T.);
#538=FACE_BOUND('',#3390,.T.);
#614=CONICAL_SURFACE('',#18116,8.5,0.78539816339745);
#615=CONICAL_SURFACE('',#18134,6.65,0.540419500270586);
#1075=CIRCLE('',#18068,2.99999999999999);
#1076=CIRCLE('',#18069,2.99999999999997);
#1077=CIRCLE('',#18070,2.99999999999999);
#1078=CIRCLE('',#18071,3.00000000000001);
#1079=CIRCLE('',#18072,3.);
#1080=CIRCLE('',#18075,2.99999999999997);
#1081=CIRCLE('',#18078,2.99999999999999);
#1082=CIRCLE('',#18081,3.00000000000001);
#1083=CIRCLE('',#18084,2.99999999999999);
#1084=CIRCLE('',#18092,5.6);
#1085=CIRCLE('',#18094,5.6);
#1086=CIRCLE('',#18096,9.);
#1087=CIRCLE('',#18098,9.);
#1088=CIRCLE('',#18100,9.);
#1089=CIRCLE('',#18102,9.);
#1090=CIRCLE('',#18103,9.);
#1091=CIRCLE('',#18105,9.);
#1092=CIRCLE('',#18107,9.);
#1093=CIRCLE('',#18109,9.);
#1094=CIRCLE('',#18110,9.);
#1095=CIRCLE('',#18111,9.);
#1096=CIRCLE('',#18112,9.);
#1097=CIRCLE('',#18113,9.);
#1098=CIRCLE('',#18114,9.);
#1099=CIRCLE('',#18115,9.);
#1100=CIRCLE('',#18117,8.);
#1101=CIRCLE('',#18125,6.8);
#1102=CIRCLE('',#18133,6.5);
#1103=CIRCLE('',#18135,6.8);
#1440=CYLINDRICAL_SURFACE('',#18074,2.99999999999997);
#1441=CYLINDRICAL_SURFACE('',#18077,2.99999999999999);
#1442=CYLINDRICAL_SURFACE('',#18080,3.00000000000001);
#1443=CYLINDRICAL_SURFACE('',#18083,2.99999999999999);
#1444=CYLINDRICAL_SURFACE('',#18086,3.);
#1445=CYLINDRICAL_SURFACE('',#18093,5.6);
#1446=CYLINDRICAL_SURFACE('',#18108,9.);
#1447=CYLINDRICAL_SURFACE('',#18136,6.8);
#2264=FACE_OUTER_BOUND('',#3359,.T.);
#2265=FACE_OUTER_BOUND('',#3361,.T.);
#2266=FACE_OUTER_BOUND('',#3362,.T.);
#2267=FACE_OUTER_BOUND('',#3363,.T.);
#2268=FACE_OUTER_BOUND('',#3364,.T.);
#2269=FACE_OUTER_BOUND('',#3365,.T.);
#2270=FACE_OUTER_BOUND('',#3366,.T.);
#2271=FACE_OUTER_BOUND('',#3367,.T.);
#2272=FACE_OUTER_BOUND('',#3368,.T.);
#2273=FACE_OUTER_BOUND('',#3369,.T.);
#2274=FACE_OUTER_BOUND('',#3370,.T.);
#2275=FACE_OUTER_BOUND('',#3371,.T.);
#2276=FACE_OUTER_BOUND('',#3372,.T.);
#2277=FACE_OUTER_BOUND('',#3373,.T.);
#2278=FACE_OUTER_BOUND('',#3374,.T.);
#2279=FACE_OUTER_BOUND('',#3375,.T.);
#2280=FACE_OUTER_BOUND('',#3376,.T.);
#2281=FACE_OUTER_BOUND('',#3377,.T.);
#2282=FACE_OUTER_BOUND('',#3378,.T.);
#2283=FACE_OUTER_BOUND('',#3379,.T.);
#2284=FACE_OUTER_BOUND('',#3380,.T.);
#2285=FACE_OUTER_BOUND('',#3381,.T.);
#2286=FACE_OUTER_BOUND('',#3382,.T.);
#2287=FACE_OUTER_BOUND('',#3384,.T.);
#2288=FACE_OUTER_BOUND('',#3385,.T.);
#2289=FACE_OUTER_BOUND('',#3386,.T.);
#2290=FACE_OUTER_BOUND('',#3387,.T.);
#2291=FACE_OUTER_BOUND('',#3388,.T.);
#2292=FACE_OUTER_BOUND('',#3389,.T.);
#2293=FACE_OUTER_BOUND('',#3391,.T.);
#2294=FACE_OUTER_BOUND('',#3392,.T.);
#2295=FACE_OUTER_BOUND('',#3393,.T.);
#2296=FACE_OUTER_BOUND('',#3394,.T.);
#2297=FACE_OUTER_BOUND('',#3395,.T.);
#2298=FACE_OUTER_BOUND('',#3396,.T.);
#2299=FACE_OUTER_BOUND('',#3397,.T.);
#2300=FACE_OUTER_BOUND('',#3398,.T.);
#2301=FACE_OUTER_BOUND('',#3399,.T.);
#3359=EDGE_LOOP('',(#13000,#13001,#13002,#13003,#13004,#13005,#13006,#13007));
#3360=EDGE_LOOP('',(#13008));
#3361=EDGE_LOOP('',(#13009,#13010,#13011,#13012));
#3362=EDGE_LOOP('',(#13013,#13014,#13015,#13016));
#3363=EDGE_LOOP('',(#13017,#13018,#13019,#13020));
#3364=EDGE_LOOP('',(#13021,#13022,#13023,#13024));
#3365=EDGE_LOOP('',(#13025,#13026,#13027,#13028));
#3366=EDGE_LOOP('',(#13029,#13030,#13031,#13032));
#3367=EDGE_LOOP('',(#13033,#13034,#13035,#13036));
#3368=EDGE_LOOP('',(#13037,#13038,#13039,#13040));
#3369=EDGE_LOOP('',(#13041,#13042,#13043,#13044,#13045,#13046,#13047,#13048));
#3370=EDGE_LOOP('',(#13049,#13050,#13051,#13052,#13053,#13054));
#3371=EDGE_LOOP('',(#13055,#13056,#13057,#13058,#13059,#13060,#13061,#13062));
#3372=EDGE_LOOP('',(#13063));
#3373=EDGE_LOOP('',(#13064,#13065,#13066,#13067));
#3374=EDGE_LOOP('',(#13068,#13069));
#3375=EDGE_LOOP('',(#13070,#13071));
#3376=EDGE_LOOP('',(#13072,#13073));
#3377=EDGE_LOOP('',(#13074,#13075,#13076));
#3378=EDGE_LOOP('',(#13077,#13078));
#3379=EDGE_LOOP('',(#13079,#13080));
#3380=EDGE_LOOP('',(#13081,#13082,#13083,#13084,#13085,#13086,#13087,#13088,
#13089,#13090,#13091,#13092,#13093,#13094,#13095,#13096));
#3381=EDGE_LOOP('',(#13097,#13098,#13099,#13100));
#3382=EDGE_LOOP('',(#13101));
#3383=EDGE_LOOP('',(#13102));
#3384=EDGE_LOOP('',(#13103,#13104,#13105));
#3385=EDGE_LOOP('',(#13106,#13107,#13108));
#3386=EDGE_LOOP('',(#13109,#13110,#13111));
#3387=EDGE_LOOP('',(#13112,#13113,#13114));
#3388=EDGE_LOOP('',(#13115,#13116,#13117));
#3389=EDGE_LOOP('',(#13118,#13119,#13120,#13121,#13122,#13123));
#3390=EDGE_LOOP('',(#13124));
#3391=EDGE_LOOP('',(#13125,#13126,#13127,#13128,#13129,#13130));
#3392=EDGE_LOOP('',(#13131,#13132,#13133,#13134,#13135,#13136));
#3393=EDGE_LOOP('',(#13137,#13138,#13139,#13140,#13141,#13142,#13143,#13144,
#13145));
#3394=EDGE_LOOP('',(#13146,#13147,#13148,#13149,#13150,#13151));
#3395=EDGE_LOOP('',(#13152,#13153,#13154,#13155,#13156,#13157));
#3396=EDGE_LOOP('',(#13158,#13159,#13160));
#3397=EDGE_LOOP('',(#13161));
#3398=EDGE_LOOP('',(#13162,#13163,#13164,#13165));
#3399=EDGE_LOOP('',(#13166,#13167,#13168,#13169));
#4303=LINE('',#36077,#5257);
#4304=LINE('',#36081,#5258);
#4305=LINE('',#36085,#5259);
#4306=LINE('',#36088,#5260);
#4307=LINE('',#36093,#5261);
#4308=LINE('',#36095,#5262);
#4309=LINE('',#36096,#5263);
#4310=LINE('',#36100,#5264);
#4311=LINE('',#36103,#5265);
#4312=LINE('',#36104,#5266);
#4313=LINE('',#36108,#5267);
#4314=LINE('',#36111,#5268);
#4315=LINE('',#36112,#5269);
#4316=LINE('',#36116,#5270);
#4317=LINE('',#36119,#5271);
#4318=LINE('',#36120,#5272);
#4319=LINE('',#36126,#5273);
#4320=LINE('',#36134,#5274);
#4321=LINE('',#36136,#5275);
#4322=LINE('',#36138,#5276);
#4323=LINE('',#36140,#5277);
#4324=LINE('',#36142,#5278);
#4325=LINE('',#36144,#5279);
#4326=LINE('',#36145,#5280);
#4327=LINE('',#36151,#5281);
#4328=LINE('',#36156,#5282);
#4329=LINE('',#36161,#5283);
#4330=LINE('',#36166,#5284);
#4331=LINE('',#36171,#5285);
#4332=LINE('',#36180,#5286);
#4333=LINE('',#36185,#5287);
#4334=LINE('',#36195,#5288);
#4335=LINE('',#36199,#5289);
#4336=LINE('',#36200,#5290);
#4337=LINE('',#36202,#5291);
#4338=LINE('',#36205,#5292);
#4339=LINE('',#36206,#5293);
#4340=LINE('',#36208,#5294);
#4341=LINE('',#36211,#5295);
#4342=LINE('',#36212,#5296);
#4343=LINE('',#36216,#5297);
#4344=LINE('',#36218,#5298);
#4345=LINE('',#36220,#5299);
#4346=LINE('',#36221,#5300);
#4347=LINE('',#36222,#5301);
#4348=LINE('',#36226,#5302);
#4349=LINE('',#36227,#5303);
#4350=LINE('',#36230,#5304);
#4351=LINE('',#36231,#5305);
#4352=LINE('',#36233,#5306);
#4353=LINE('',#36235,#5307);
#4354=LINE('',#36244,#5308);
#4355=LINE('',#36246,#5309);
#5257=VECTOR('',#20949,10.);
#5258=VECTOR('',#20952,10.);
#5259=VECTOR('',#20955,10.);
#5260=VECTOR('',#20958,10.);
#5261=VECTOR('',#20963,10.);
#5262=VECTOR('',#20964,10.);
#5263=VECTOR('',#20965,10.);
#5264=VECTOR('',#20970,10.);
#5265=VECTOR('',#20973,10.);
#5266=VECTOR('',#20974,10.);
#5267=VECTOR('',#20979,10.);
#5268=VECTOR('',#20982,10.);
#5269=VECTOR('',#20983,10.);
#5270=VECTOR('',#20988,10.);
#5271=VECTOR('',#20991,10.);
#5272=VECTOR('',#20992,10.);
#5273=VECTOR('',#21001,3.);
#5274=VECTOR('',#21010,10.);
#5275=VECTOR('',#21011,10.);
#5276=VECTOR('',#21012,10.);
#5277=VECTOR('',#21013,10.);
#5278=VECTOR('',#21014,10.);
#5279=VECTOR('',#21015,10.);
#5280=VECTOR('',#21016,10.);
#5281=VECTOR('',#21023,5.6);
#5282=VECTOR('',#21028,10.);
#5283=VECTOR('',#21033,10.);
#5284=VECTOR('',#21038,10.);
#5285=VECTOR('',#21043,10.);
#5286=VECTOR('',#21054,10.);
#5287=VECTOR('',#21061,9.);
#5288=VECTOR('',#21078,8.5);
#5289=VECTOR('',#21083,10.);
#5290=VECTOR('',#21084,10.);
#5291=VECTOR('',#21087,10.);
#5292=VECTOR('',#21090,10.);
#5293=VECTOR('',#21091,10.);
#5294=VECTOR('',#21094,10.);
#5295=VECTOR('',#21097,10.);
#5296=VECTOR('',#21098,10.);
#5297=VECTOR('',#21101,10.);
#5298=VECTOR('',#21102,10.);
#5299=VECTOR('',#21103,10.);
#5300=VECTOR('',#21104,10.);
#5301=VECTOR('',#21105,10.);
#5302=VECTOR('',#21110,10.);
#5303=VECTOR('',#21111,10.);
#5304=VECTOR('',#21114,10.);
#5305=VECTOR('',#21115,10.);
#5306=VECTOR('',#21118,10.);
#5307=VECTOR('',#21121,10.);
#5308=VECTOR('',#21134,6.65);
#5309=VECTOR('',#21137,6.8);
#7416=VERTEX_POINT('',#36073);
#7417=VERTEX_POINT('',#36074);
#7418=VERTEX_POINT('',#36076);
#7419=VERTEX_POINT('',#36078);
#7420=VERTEX_POINT('',#36080);
#7421=VERTEX_POINT('',#36082);
#7422=VERTEX_POINT('',#36084);
#7423=VERTEX_POINT('',#36086);
#7424=VERTEX_POINT('',#36089);
#7425=VERTEX_POINT('',#36092);
#7426=VERTEX_POINT('',#36094);
#7427=VERTEX_POINT('',#36098);
#7428=VERTEX_POINT('',#36102);
#7429=VERTEX_POINT('',#36106);
#7430=VERTEX_POINT('',#36110);
#7431=VERTEX_POINT('',#36114);
#7432=VERTEX_POINT('',#36118);
#7433=VERTEX_POINT('',#36125);
#7434=VERTEX_POINT('',#36127);
#7435=VERTEX_POINT('',#36129);
#7436=VERTEX_POINT('',#36133);
#7437=VERTEX_POINT('',#36135);
#7438=VERTEX_POINT('',#36137);
#7439=VERTEX_POINT('',#36139);
#7440=VERTEX_POINT('',#36141);
#7441=VERTEX_POINT('',#36143);
#7442=VERTEX_POINT('',#36147);
#7443=VERTEX_POINT('',#36150);
#7444=VERTEX_POINT('',#36154);
#7445=VERTEX_POINT('',#36155);
#7446=VERTEX_POINT('',#36159);
#7447=VERTEX_POINT('',#36160);
#7448=VERTEX_POINT('',#36164);
#7449=VERTEX_POINT('',#36165);
#7450=VERTEX_POINT('',#36169);
#7451=VERTEX_POINT('',#36170);
#7452=VERTEX_POINT('',#36172);
#7453=VERTEX_POINT('',#36178);
#7454=VERTEX_POINT('',#36179);
#7455=VERTEX_POINT('',#36183);
#7456=VERTEX_POINT('',#36193);
#7457=VERTEX_POINT('',#36198);
#7458=VERTEX_POINT('',#36204);
#7459=VERTEX_POINT('',#36210);
#7460=VERTEX_POINT('',#36214);
#7461=VERTEX_POINT('',#36215);
#7462=VERTEX_POINT('',#36217);
#7463=VERTEX_POINT('',#36219);
#7464=VERTEX_POINT('',#36223);
#7465=VERTEX_POINT('',#36229);
#7466=VERTEX_POINT('',#36239);
#7467=VERTEX_POINT('',#36242);
#9407=EDGE_CURVE('',#7416,#7417,#1075,.T.);
#9408=EDGE_CURVE('',#7418,#7416,#4303,.T.);
#9409=EDGE_CURVE('',#7419,#7418,#1076,.T.);
#9410=EDGE_CURVE('',#7420,#7419,#4304,.T.);
#9411=EDGE_CURVE('',#7421,#7420,#1077,.T.);
#9412=EDGE_CURVE('',#7422,#7421,#4305,.T.);
#9413=EDGE_CURVE('',#7423,#7422,#1078,.T.);
#9414=EDGE_CURVE('',#7417,#7423,#4306,.T.);
#9415=EDGE_CURVE('',#7424,#7424,#1079,.T.);
#9416=EDGE_CURVE('',#7416,#7425,#4307,.T.);
#9417=EDGE_CURVE('',#7426,#7425,#4308,.T.);
#9418=EDGE_CURVE('',#7418,#7426,#4309,.T.);
#9419=EDGE_CURVE('',#7427,#7426,#1080,.T.);
#9420=EDGE_CURVE('',#7419,#7427,#4310,.T.);
#9421=EDGE_CURVE('',#7428,#7427,#4311,.T.);
#9422=EDGE_CURVE('',#7420,#7428,#4312,.T.);
#9423=EDGE_CURVE('',#7429,#7428,#1081,.T.);
#9424=EDGE_CURVE('',#7421,#7429,#4313,.T.);
#9425=EDGE_CURVE('',#7430,#7429,#4314,.T.);
#9426=EDGE_CURVE('',#7422,#7430,#4315,.T.);
#9427=EDGE_CURVE('',#7431,#7430,#1082,.T.);
#9428=EDGE_CURVE('',#7423,#7431,#4316,.T.);
#9429=EDGE_CURVE('',#7432,#7431,#4317,.T.);
#9430=EDGE_CURVE('',#7417,#7432,#4318,.T.);
#9431=EDGE_CURVE('',#7425,#7432,#1083,.T.);
#9432=EDGE_CURVE('',#7424,#7433,#4319,.T.);
#9433=EDGE_CURVE('',#7434,#7433,#254,.T.);
#9434=EDGE_CURVE('',#7435,#7434,#255,.T.);
#9435=EDGE_CURVE('',#7433,#7435,#256,.T.);
#9436=EDGE_CURVE('',#7434,#7436,#4320,.T.);
#9437=EDGE_CURVE('',#7437,#7436,#4321,.T.);
#9438=EDGE_CURVE('',#7438,#7437,#4322,.T.);
#9439=EDGE_CURVE('',#7439,#7438,#4323,.T.);
#9440=EDGE_CURVE('',#7440,#7439,#4324,.T.);
#9441=EDGE_CURVE('',#7440,#7441,#4325,.T.);
#9442=EDGE_CURVE('',#7441,#7435,#4326,.T.);
#9443=EDGE_CURVE('',#7442,#7442,#1084,.T.);
#9444=EDGE_CURVE('',#7442,#7443,#4327,.T.);
#9445=EDGE_CURVE('',#7443,#7443,#1085,.T.);
#9446=EDGE_CURVE('',#7444,#7445,#4328,.T.);
#9447=EDGE_CURVE('',#7444,#7445,#1086,.T.);
#9448=EDGE_CURVE('',#7446,#7447,#4329,.T.);
#9449=EDGE_CURVE('',#7446,#7447,#1087,.T.);
#9450=EDGE_CURVE('',#7448,#7449,#4330,.T.);
#9451=EDGE_CURVE('',#7448,#7449,#1088,.T.);
#9452=EDGE_CURVE('',#7450,#7451,#4331,.T.);
#9453=EDGE_CURVE('',#7452,#7451,#1089,.T.);
#9454=EDGE_CURVE('',#7450,#7452,#1090,.T.);
#9455=EDGE_CURVE('',#7438,#7437,#1091,.T.);
#9456=EDGE_CURVE('',#7453,#7454,#4332,.T.);
#9457=EDGE_CURVE('',#7453,#7454,#1092,.T.);
#9458=EDGE_CURVE('',#7455,#7455,#1093,.T.);
#9459=EDGE_CURVE('',#7455,#7452,#4333,.T.);
#9460=EDGE_CURVE('',#7446,#7451,#1094,.T.);
#9461=EDGE_CURVE('',#7444,#7447,#1095,.T.);
#9462=EDGE_CURVE('',#7448,#7445,#1096,.T.);
#9463=EDGE_CURVE('',#7438,#7449,#1097,.T.);
#9464=EDGE_CURVE('',#7453,#7437,#1098,.T.);
#9465=EDGE_CURVE('',#7450,#7454,#1099,.T.);
#9466=EDGE_CURVE('',#7456,#7456,#1100,.T.);
#9467=EDGE_CURVE('',#7456,#7455,#4334,.T.);
#9468=EDGE_CURVE('',#7445,#7457,#4335,.T.);
#9469=EDGE_CURVE('',#7457,#7448,#4336,.T.);
#9470=EDGE_CURVE('',#7449,#7439,#4337,.T.);
#9471=EDGE_CURVE('',#7447,#7458,#4338,.T.);
#9472=EDGE_CURVE('',#7458,#7444,#4339,.T.);
#9473=EDGE_CURVE('',#7436,#7453,#4340,.T.);
#9474=EDGE_CURVE('',#7451,#7459,#4341,.T.);
#9475=EDGE_CURVE('',#7459,#7446,#4342,.T.);
#9476=EDGE_CURVE('',#7460,#7461,#4343,.T.);
#9477=EDGE_CURVE('',#7462,#7460,#4344,.T.);
#9478=EDGE_CURVE('',#7463,#7462,#4345,.T.);
#9479=EDGE_CURVE('',#7441,#7463,#4346,.T.);
#9480=EDGE_CURVE('',#7461,#7440,#4347,.T.);
#9481=EDGE_CURVE('',#7464,#7464,#1101,.T.);
#9482=EDGE_CURVE('',#7460,#7458,#4348,.T.);
#9483=EDGE_CURVE('',#7462,#7459,#4349,.T.);
#9484=EDGE_CURVE('',#7465,#7450,#4350,.T.);
#9485=EDGE_CURVE('',#7463,#7465,#4351,.T.);
#9486=EDGE_CURVE('',#7454,#7465,#4352,.T.);
#9487=EDGE_CURVE('',#7461,#7457,#4353,.T.);
#9488=EDGE_CURVE('',#7466,#7466,#1102,.T.);
#9489=EDGE_CURVE('',#7467,#7467,#1103,.T.);
#9490=EDGE_CURVE('',#7467,#7466,#4354,.T.);
#9491=EDGE_CURVE('',#7464,#7467,#4355,.T.);
#13000=ORIENTED_EDGE('',*,*,#9407,.F.);
#13001=ORIENTED_EDGE('',*,*,#9408,.F.);
#13002=ORIENTED_EDGE('',*,*,#9409,.F.);
#13003=ORIENTED_EDGE('',*,*,#9410,.F.);
#13004=ORIENTED_EDGE('',*,*,#9411,.F.);
#13005=ORIENTED_EDGE('',*,*,#9412,.F.);
#13006=ORIENTED_EDGE('',*,*,#9413,.F.);
#13007=ORIENTED_EDGE('',*,*,#9414,.F.);
#13008=ORIENTED_EDGE('',*,*,#9415,.T.);
#13009=ORIENTED_EDGE('',*,*,#9408,.T.);
#13010=ORIENTED_EDGE('',*,*,#9416,.T.);
#13011=ORIENTED_EDGE('',*,*,#9417,.F.);
#13012=ORIENTED_EDGE('',*,*,#9418,.F.);
#13013=ORIENTED_EDGE('',*,*,#9409,.T.);
#13014=ORIENTED_EDGE('',*,*,#9418,.T.);
#13015=ORIENTED_EDGE('',*,*,#9419,.F.);
#13016=ORIENTED_EDGE('',*,*,#9420,.F.);
#13017=ORIENTED_EDGE('',*,*,#9410,.T.);
#13018=ORIENTED_EDGE('',*,*,#9420,.T.);
#13019=ORIENTED_EDGE('',*,*,#9421,.F.);
#13020=ORIENTED_EDGE('',*,*,#9422,.F.);
#13021=ORIENTED_EDGE('',*,*,#9411,.T.);
#13022=ORIENTED_EDGE('',*,*,#9422,.T.);
#13023=ORIENTED_EDGE('',*,*,#9423,.F.);
#13024=ORIENTED_EDGE('',*,*,#9424,.F.);
#13025=ORIENTED_EDGE('',*,*,#9412,.T.);
#13026=ORIENTED_EDGE('',*,*,#9424,.T.);
#13027=ORIENTED_EDGE('',*,*,#9425,.F.);
#13028=ORIENTED_EDGE('',*,*,#9426,.F.);
#13029=ORIENTED_EDGE('',*,*,#9413,.T.);
#13030=ORIENTED_EDGE('',*,*,#9426,.T.);
#13031=ORIENTED_EDGE('',*,*,#9427,.F.);
#13032=ORIENTED_EDGE('',*,*,#9428,.F.);
#13033=ORIENTED_EDGE('',*,*,#9414,.T.);
#13034=ORIENTED_EDGE('',*,*,#9428,.T.);
#13035=ORIENTED_EDGE('',*,*,#9429,.F.);
#13036=ORIENTED_EDGE('',*,*,#9430,.F.);
#13037=ORIENTED_EDGE('',*,*,#9407,.T.);
#13038=ORIENTED_EDGE('',*,*,#9430,.T.);
#13039=ORIENTED_EDGE('',*,*,#9431,.F.);
#13040=ORIENTED_EDGE('',*,*,#9416,.F.);
#13041=ORIENTED_EDGE('',*,*,#9431,.T.);
#13042=ORIENTED_EDGE('',*,*,#9429,.T.);
#13043=ORIENTED_EDGE('',*,*,#9427,.T.);
#13044=ORIENTED_EDGE('',*,*,#9425,.T.);
#13045=ORIENTED_EDGE('',*,*,#9423,.T.);
#13046=ORIENTED_EDGE('',*,*,#9421,.T.);
#13047=ORIENTED_EDGE('',*,*,#9419,.T.);
#13048=ORIENTED_EDGE('',*,*,#9417,.T.);
#13049=ORIENTED_EDGE('',*,*,#9415,.F.);
#13050=ORIENTED_EDGE('',*,*,#9432,.T.);
#13051=ORIENTED_EDGE('',*,*,#9433,.F.);
#13052=ORIENTED_EDGE('',*,*,#9434,.F.);
#13053=ORIENTED_EDGE('',*,*,#9435,.F.);
#13054=ORIENTED_EDGE('',*,*,#9432,.F.);
#13055=ORIENTED_EDGE('',*,*,#9434,.T.);
#13056=ORIENTED_EDGE('',*,*,#9436,.T.);
#13057=ORIENTED_EDGE('',*,*,#9437,.F.);
#13058=ORIENTED_EDGE('',*,*,#9438,.F.);
#13059=ORIENTED_EDGE('',*,*,#9439,.F.);
#13060=ORIENTED_EDGE('',*,*,#9440,.F.);
#13061=ORIENTED_EDGE('',*,*,#9441,.T.);
#13062=ORIENTED_EDGE('',*,*,#9442,.T.);
#13063=ORIENTED_EDGE('',*,*,#9443,.T.);
#13064=ORIENTED_EDGE('',*,*,#9443,.F.);
#13065=ORIENTED_EDGE('',*,*,#9444,.T.);
#13066=ORIENTED_EDGE('',*,*,#9445,.F.);
#13067=ORIENTED_EDGE('',*,*,#9444,.F.);
#13068=ORIENTED_EDGE('',*,*,#9446,.T.);
#13069=ORIENTED_EDGE('',*,*,#9447,.F.);
#13070=ORIENTED_EDGE('',*,*,#9448,.T.);
#13071=ORIENTED_EDGE('',*,*,#9449,.F.);
#13072=ORIENTED_EDGE('',*,*,#9450,.T.);
#13073=ORIENTED_EDGE('',*,*,#9451,.F.);
#13074=ORIENTED_EDGE('',*,*,#9452,.T.);
#13075=ORIENTED_EDGE('',*,*,#9453,.F.);
#13076=ORIENTED_EDGE('',*,*,#9454,.F.);
#13077=ORIENTED_EDGE('',*,*,#9438,.T.);
#13078=ORIENTED_EDGE('',*,*,#9455,.F.);
#13079=ORIENTED_EDGE('',*,*,#9456,.T.);
#13080=ORIENTED_EDGE('',*,*,#9457,.F.);
#13081=ORIENTED_EDGE('',*,*,#9458,.F.);
#13082=ORIENTED_EDGE('',*,*,#9459,.T.);
#13083=ORIENTED_EDGE('',*,*,#9453,.T.);
#13084=ORIENTED_EDGE('',*,*,#9460,.F.);
#13085=ORIENTED_EDGE('',*,*,#9449,.T.);
#13086=ORIENTED_EDGE('',*,*,#9461,.F.);
#13087=ORIENTED_EDGE('',*,*,#9447,.T.);
#13088=ORIENTED_EDGE('',*,*,#9462,.F.);
#13089=ORIENTED_EDGE('',*,*,#9451,.T.);
#13090=ORIENTED_EDGE('',*,*,#9463,.F.);
#13091=ORIENTED_EDGE('',*,*,#9455,.T.);
#13092=ORIENTED_EDGE('',*,*,#9464,.F.);
#13093=ORIENTED_EDGE('',*,*,#9457,.T.);
#13094=ORIENTED_EDGE('',*,*,#9465,.F.);
#13095=ORIENTED_EDGE('',*,*,#9454,.T.);
#13096=ORIENTED_EDGE('',*,*,#9459,.F.);
#13097=ORIENTED_EDGE('',*,*,#9466,.F.);
#13098=ORIENTED_EDGE('',*,*,#9467,.T.);
#13099=ORIENTED_EDGE('',*,*,#9458,.T.);
#13100=ORIENTED_EDGE('',*,*,#9467,.F.);
#13101=ORIENTED_EDGE('',*,*,#9466,.T.);
#13102=ORIENTED_EDGE('',*,*,#9445,.T.);
#13103=ORIENTED_EDGE('',*,*,#9462,.T.);
#13104=ORIENTED_EDGE('',*,*,#9468,.T.);
#13105=ORIENTED_EDGE('',*,*,#9469,.T.);
#13106=ORIENTED_EDGE('',*,*,#9463,.T.);
#13107=ORIENTED_EDGE('',*,*,#9470,.T.);
#13108=ORIENTED_EDGE('',*,*,#9439,.T.);
#13109=ORIENTED_EDGE('',*,*,#9461,.T.);
#13110=ORIENTED_EDGE('',*,*,#9471,.T.);
#13111=ORIENTED_EDGE('',*,*,#9472,.T.);
#13112=ORIENTED_EDGE('',*,*,#9464,.T.);
#13113=ORIENTED_EDGE('',*,*,#9437,.T.);
#13114=ORIENTED_EDGE('',*,*,#9473,.T.);
#13115=ORIENTED_EDGE('',*,*,#9460,.T.);
#13116=ORIENTED_EDGE('',*,*,#9474,.T.);
#13117=ORIENTED_EDGE('',*,*,#9475,.T.);
#13118=ORIENTED_EDGE('',*,*,#9476,.F.);
#13119=ORIENTED_EDGE('',*,*,#9477,.F.);
#13120=ORIENTED_EDGE('',*,*,#9478,.F.);
#13121=ORIENTED_EDGE('',*,*,#9479,.F.);
#13122=ORIENTED_EDGE('',*,*,#9441,.F.);
#13123=ORIENTED_EDGE('',*,*,#9480,.F.);
#13124=ORIENTED_EDGE('',*,*,#9481,.T.);
#13125=ORIENTED_EDGE('',*,*,#9477,.T.);
#13126=ORIENTED_EDGE('',*,*,#9482,.T.);
#13127=ORIENTED_EDGE('',*,*,#9471,.F.);
#13128=ORIENTED_EDGE('',*,*,#9448,.F.);
#13129=ORIENTED_EDGE('',*,*,#9475,.F.);
#13130=ORIENTED_EDGE('',*,*,#9483,.F.);
#13131=ORIENTED_EDGE('',*,*,#9478,.T.);
#13132=ORIENTED_EDGE('',*,*,#9483,.T.);
#13133=ORIENTED_EDGE('',*,*,#9474,.F.);
#13134=ORIENTED_EDGE('',*,*,#9452,.F.);
#13135=ORIENTED_EDGE('',*,*,#9484,.F.);
#13136=ORIENTED_EDGE('',*,*,#9485,.F.);
#13137=ORIENTED_EDGE('',*,*,#9433,.T.);
#13138=ORIENTED_EDGE('',*,*,#9435,.T.);
#13139=ORIENTED_EDGE('',*,*,#9442,.F.);
#13140=ORIENTED_EDGE('',*,*,#9479,.T.);
#13141=ORIENTED_EDGE('',*,*,#9485,.T.);
#13142=ORIENTED_EDGE('',*,*,#9486,.F.);
#13143=ORIENTED_EDGE('',*,*,#9456,.F.);
#13144=ORIENTED_EDGE('',*,*,#9473,.F.);
#13145=ORIENTED_EDGE('',*,*,#9436,.F.);
#13146=ORIENTED_EDGE('',*,*,#9480,.T.);
#13147=ORIENTED_EDGE('',*,*,#9440,.T.);
#13148=ORIENTED_EDGE('',*,*,#9470,.F.);
#13149=ORIENTED_EDGE('',*,*,#9450,.F.);
#13150=ORIENTED_EDGE('',*,*,#9469,.F.);
#13151=ORIENTED_EDGE('',*,*,#9487,.F.);
#13152=ORIENTED_EDGE('',*,*,#9476,.T.);
#13153=ORIENTED_EDGE('',*,*,#9487,.T.);
#13154=ORIENTED_EDGE('',*,*,#9468,.F.);
#13155=ORIENTED_EDGE('',*,*,#9446,.F.);
#13156=ORIENTED_EDGE('',*,*,#9472,.F.);
#13157=ORIENTED_EDGE('',*,*,#9482,.F.);
#13158=ORIENTED_EDGE('',*,*,#9465,.T.);
#13159=ORIENTED_EDGE('',*,*,#9486,.T.);
#13160=ORIENTED_EDGE('',*,*,#9484,.T.);
#13161=ORIENTED_EDGE('',*,*,#9488,.F.);
#13162=ORIENTED_EDGE('',*,*,#9489,.F.);
#13163=ORIENTED_EDGE('',*,*,#9490,.T.);
#13164=ORIENTED_EDGE('',*,*,#9488,.T.);
#13165=ORIENTED_EDGE('',*,*,#9490,.F.);
#13166=ORIENTED_EDGE('',*,*,#9481,.F.);
#13167=ORIENTED_EDGE('',*,*,#9491,.T.);
#13168=ORIENTED_EDGE('',*,*,#9489,.T.);
#13169=ORIENTED_EDGE('',*,*,#9491,.F.);
#15844=PLANE('',#18067);
#15845=PLANE('',#18073);
#15846=PLANE('',#18076);
#15847=PLANE('',#18079);
#15848=PLANE('',#18082);
#15849=PLANE('',#18085);
#15850=PLANE('',#18090);
#15851=PLANE('',#18091);
#15852=PLANE('',#18095);
#15853=PLANE('',#18097);
#15854=PLANE('',#18099);
#15855=PLANE('',#18101);
#15856=PLANE('',#18104);
#15857=PLANE('',#18106);
#15858=PLANE('',#18118);
#15859=PLANE('',#18119);
#15860=PLANE('',#18120);
#15861=PLANE('',#18121);
#15862=PLANE('',#18122);
#15863=PLANE('',#18123);
#15864=PLANE('',#18124);
#15865=PLANE('',#18126);
#15866=PLANE('',#18127);
#15867=PLANE('',#18128);
#15868=PLANE('',#18129);
#15869=PLANE('',#18130);
#15870=PLANE('',#18131);
#15871=PLANE('',#18132);
#16435=ADVANCED_FACE('',(#2264,#536),#15844,.F.);
#16436=ADVANCED_FACE('',(#2265),#15845,.T.);
#16437=ADVANCED_FACE('',(#2266),#1440,.T.);
#16438=ADVANCED_FACE('',(#2267),#15846,.T.);
#16439=ADVANCED_FACE('',(#2268),#1441,.T.);
#16440=ADVANCED_FACE('',(#2269),#15847,.T.);
#16441=ADVANCED_FACE('',(#2270),#1442,.T.);
#16442=ADVANCED_FACE('',(#2271),#15848,.T.);
#16443=ADVANCED_FACE('',(#2272),#1443,.T.);
#16444=ADVANCED_FACE('',(#2273),#15849,.T.);
#16445=ADVANCED_FACE('',(#2274),#1444,.T.);
#16446=ADVANCED_FACE('',(#2275),#15850,.T.);
#16447=ADVANCED_FACE('',(#2276),#15851,.F.);
#16448=ADVANCED_FACE('',(#2277),#1445,.F.);
#16449=ADVANCED_FACE('',(#2278),#15852,.T.);
#16450=ADVANCED_FACE('',(#2279),#15853,.T.);
#16451=ADVANCED_FACE('',(#2280),#15854,.T.);
#16452=ADVANCED_FACE('',(#2281),#15855,.T.);
#16453=ADVANCED_FACE('',(#2282),#15856,.T.);
#16454=ADVANCED_FACE('',(#2283),#15857,.T.);
#16455=ADVANCED_FACE('',(#2284),#1446,.T.);
#16456=ADVANCED_FACE('',(#2285),#614,.T.);
#16457=ADVANCED_FACE('',(#2286,#537),#15858,.T.);
#16458=ADVANCED_FACE('',(#2287),#15859,.T.);
#16459=ADVANCED_FACE('',(#2288),#15860,.T.);
#16460=ADVANCED_FACE('',(#2289),#15861,.T.);
#16461=ADVANCED_FACE('',(#2290),#15862,.T.);
#16462=ADVANCED_FACE('',(#2291),#15863,.T.);
#16463=ADVANCED_FACE('',(#2292,#538),#15864,.T.);
#16464=ADVANCED_FACE('',(#2293),#15865,.T.);
#16465=ADVANCED_FACE('',(#2294),#15866,.T.);
#16466=ADVANCED_FACE('',(#2295),#15867,.T.);
#16467=ADVANCED_FACE('',(#2296),#15868,.T.);
#16468=ADVANCED_FACE('',(#2297),#15869,.T.);
#16469=ADVANCED_FACE('',(#2298),#15870,.T.);
#16470=ADVANCED_FACE('',(#2299),#15871,.T.);
#16471=ADVANCED_FACE('',(#2300),#615,.T.);
#16472=ADVANCED_FACE('',(#2301),#1447,.T.);
#16960=CLOSED_SHELL('',(#16435,#16436,#16437,#16438,#16439,#16440,#16441,
#16442,#16443,#16444,#16445,#16446,#16447,#16448,#16449,#16450,#16451,#16452,
#16453,#16454,#16455,#16456,#16457,#16458,#16459,#16460,#16461,#16462,#16463,
#16464,#16465,#16466,#16467,#16468,#16469,#16470,#16471,#16472));
#18066=AXIS2_PLACEMENT_3D('',#36071,#20943,#20944);
#18067=AXIS2_PLACEMENT_3D('',#36072,#20945,#20946);
#18068=AXIS2_PLACEMENT_3D('',#36075,#20947,#20948);
#18069=AXIS2_PLACEMENT_3D('',#36079,#20950,#20951);
#18070=AXIS2_PLACEMENT_3D('',#36083,#20953,#20954);
#18071=AXIS2_PLACEMENT_3D('',#36087,#20956,#20957);
#18072=AXIS2_PLACEMENT_3D('',#36090,#20959,#20960);
#18073=AXIS2_PLACEMENT_3D('',#36091,#20961,#20962);
#18074=AXIS2_PLACEMENT_3D('',#36097,#20966,#20967);
#18075=AXIS2_PLACEMENT_3D('',#36099,#20968,#20969);
#18076=AXIS2_PLACEMENT_3D('',#36101,#20971,#20972);
#18077=AXIS2_PLACEMENT_3D('',#36105,#20975,#20976);
#18078=AXIS2_PLACEMENT_3D('',#36107,#20977,#20978);
#18079=AXIS2_PLACEMENT_3D('',#36109,#20980,#20981);
#18080=AXIS2_PLACEMENT_3D('',#36113,#20984,#20985);
#18081=AXIS2_PLACEMENT_3D('',#36115,#20986,#20987);
#18082=AXIS2_PLACEMENT_3D('',#36117,#20989,#20990);
#18083=AXIS2_PLACEMENT_3D('',#36121,#20993,#20994);
#18084=AXIS2_PLACEMENT_3D('',#36122,#20995,#20996);
#18085=AXIS2_PLACEMENT_3D('',#36123,#20997,#20998);
#18086=AXIS2_PLACEMENT_3D('',#36124,#20999,#21000);
#18087=AXIS2_PLACEMENT_3D('',#36128,#21002,#21003);
#18088=AXIS2_PLACEMENT_3D('',#36130,#21004,#21005);
#18089=AXIS2_PLACEMENT_3D('',#36131,#21006,#21007);
#18090=AXIS2_PLACEMENT_3D('',#36132,#21008,#21009);
#18091=AXIS2_PLACEMENT_3D('',#36146,#21017,#21018);
#18092=AXIS2_PLACEMENT_3D('',#36148,#21019,#21020);
#18093=AXIS2_PLACEMENT_3D('',#36149,#21021,#21022);
#18094=AXIS2_PLACEMENT_3D('',#36152,#21024,#21025);
#18095=AXIS2_PLACEMENT_3D('',#36153,#21026,#21027);
#18096=AXIS2_PLACEMENT_3D('',#36157,#21029,#21030);
#18097=AXIS2_PLACEMENT_3D('',#36158,#21031,#21032);
#18098=AXIS2_PLACEMENT_3D('',#36162,#21034,#21035);
#18099=AXIS2_PLACEMENT_3D('',#36163,#21036,#21037);
#18100=AXIS2_PLACEMENT_3D('',#36167,#21039,#21040);
#18101=AXIS2_PLACEMENT_3D('',#36168,#21041,#21042);
#18102=AXIS2_PLACEMENT_3D('',#36173,#21044,#21045);
#18103=AXIS2_PLACEMENT_3D('',#36174,#21046,#21047);
#18104=AXIS2_PLACEMENT_3D('',#36175,#21048,#21049);
#18105=AXIS2_PLACEMENT_3D('',#36176,#21050,#21051);
#18106=AXIS2_PLACEMENT_3D('',#36177,#21052,#21053);
#18107=AXIS2_PLACEMENT_3D('',#36181,#21055,#21056);
#18108=AXIS2_PLACEMENT_3D('',#36182,#21057,#21058);
#18109=AXIS2_PLACEMENT_3D('',#36184,#21059,#21060);
#18110=AXIS2_PLACEMENT_3D('',#36186,#21062,#21063);
#18111=AXIS2_PLACEMENT_3D('',#36187,#21064,#21065);
#18112=AXIS2_PLACEMENT_3D('',#36188,#21066,#21067);
#18113=AXIS2_PLACEMENT_3D('',#36189,#21068,#21069);
#18114=AXIS2_PLACEMENT_3D('',#36190,#21070,#21071);
#18115=AXIS2_PLACEMENT_3D('',#36191,#21072,#21073);
#18116=AXIS2_PLACEMENT_3D('',#36192,#21074,#21075);
#18117=AXIS2_PLACEMENT_3D('',#36194,#21076,#21077);
#18118=AXIS2_PLACEMENT_3D('',#36196,#21079,#21080);
#18119=AXIS2_PLACEMENT_3D('',#36197,#21081,#21082);
#18120=AXIS2_PLACEMENT_3D('',#36201,#21085,#21086);
#18121=AXIS2_PLACEMENT_3D('',#36203,#21088,#21089);
#18122=AXIS2_PLACEMENT_3D('',#36207,#21092,#21093);
#18123=AXIS2_PLACEMENT_3D('',#36209,#21095,#21096);
#18124=AXIS2_PLACEMENT_3D('',#36213,#21099,#21100);
#18125=AXIS2_PLACEMENT_3D('',#36224,#21106,#21107);
#18126=AXIS2_PLACEMENT_3D('',#36225,#21108,#21109);
#18127=AXIS2_PLACEMENT_3D('',#36228,#21112,#21113);
#18128=AXIS2_PLACEMENT_3D('',#36232,#21116,#21117);
#18129=AXIS2_PLACEMENT_3D('',#36234,#21119,#21120);
#18130=AXIS2_PLACEMENT_3D('',#36236,#21122,#21123);
#18131=AXIS2_PLACEMENT_3D('',#36237,#21124,#21125);
#18132=AXIS2_PLACEMENT_3D('',#36238,#21126,#21127);
#18133=AXIS2_PLACEMENT_3D('',#36240,#21128,#21129);
#18134=AXIS2_PLACEMENT_3D('',#36241,#21130,#21131);
#18135=AXIS2_PLACEMENT_3D('',#36243,#21132,#21133);
#18136=AXIS2_PLACEMENT_3D('',#36245,#21135,#21136);
#20943=DIRECTION('axis',(0.,0.,1.));
#20944=DIRECTION('refdir',(1.,0.,0.));
#20945=DIRECTION('center_axis',(0.,0.,1.));
#20946=DIRECTION('ref_axis',(1.,0.,0.));
#20947=DIRECTION('center_axis',(0.,0.,1.));
#20948=DIRECTION('ref_axis',(-1.,2.96059473233376E-15,0.));
#20949=DIRECTION('',(0.,-1.,0.));
#20950=DIRECTION('center_axis',(0.,0.,1.));
#20951=DIRECTION('ref_axis',(8.88178419700134E-15,1.,0.));
#20952=DIRECTION('',(-1.,0.,0.));
#20953=DIRECTION('center_axis',(0.,0.,1.));
#20954=DIRECTION('ref_axis',(1.,-5.92118946466753E-15,0.));
#20955=DIRECTION('',(0.,1.,0.));
#20956=DIRECTION('center_axis',(0.,0.,1.));
#20957=DIRECTION('ref_axis',(1.48029736616687E-15,-1.,0.));
#20958=DIRECTION('',(1.,0.,0.));
#20959=DIRECTION('center_axis',(0.,0.,1.));
#20960=DIRECTION('ref_axis',(1.,0.,0.));
#20961=DIRECTION('center_axis',(-1.,0.,0.));
#20962=DIRECTION('ref_axis',(0.,-1.,0.));
#20963=DIRECTION('',(0.,0.,1.));
#20964=DIRECTION('',(0.,-1.,0.));
#20965=DIRECTION('',(0.,0.,1.));
#20966=DIRECTION('center_axis',(0.,0.,1.));
#20967=DIRECTION('ref_axis',(8.88178419700134E-15,1.,0.));
#20968=DIRECTION('center_axis',(0.,0.,1.));
#20969=DIRECTION('ref_axis',(8.88178419700134E-15,1.,0.));
#20970=DIRECTION('',(0.,0.,1.));
#20971=DIRECTION('center_axis',(0.,1.,0.));
#20972=DIRECTION('ref_axis',(-1.,0.,0.));
#20973=DIRECTION('',(-1.,0.,0.));
#20974=DIRECTION('',(0.,0.,1.));
#20975=DIRECTION('center_axis',(0.,0.,1.));
#20976=DIRECTION('ref_axis',(1.,-5.92118946466753E-15,0.));
#20977=DIRECTION('center_axis',(0.,0.,1.));
#20978=DIRECTION('ref_axis',(1.,-5.92118946466753E-15,0.));
#20979=DIRECTION('',(0.,0.,1.));
#20980=DIRECTION('center_axis',(1.,0.,0.));
#20981=DIRECTION('ref_axis',(0.,1.,0.));
#20982=DIRECTION('',(0.,1.,0.));
#20983=DIRECTION('',(0.,0.,1.));
#20984=DIRECTION('center_axis',(0.,0.,1.));
#20985=DIRECTION('ref_axis',(1.48029736616687E-15,-1.,0.));
#20986=DIRECTION('center_axis',(0.,0.,1.));
#20987=DIRECTION('ref_axis',(1.48029736616687E-15,-1.,0.));
#20988=DIRECTION('',(0.,0.,1.));
#20989=DIRECTION('center_axis',(0.,-1.,0.));
#20990=DIRECTION('ref_axis',(1.,0.,0.));
#20991=DIRECTION('',(1.,0.,0.));
#20992=DIRECTION('',(0.,0.,1.));
#20993=DIRECTION('center_axis',(0.,0.,1.));
#20994=DIRECTION('ref_axis',(-1.,2.96059473233376E-15,0.));
#20995=DIRECTION('center_axis',(0.,0.,1.));
#20996=DIRECTION('ref_axis',(-1.,2.96059473233376E-15,0.));
#20997=DIRECTION('center_axis',(0.,0.,1.));
#20998=DIRECTION('ref_axis',(1.,0.,0.));
#20999=DIRECTION('center_axis',(0.,0.,1.));
#21000=DIRECTION('ref_axis',(1.,0.,0.));
#21001=DIRECTION('',(0.,0.,-1.));
#21002=DIRECTION('center_axis',(0.5,0.,-0.866025403784438));
#21003=DIRECTION('ref_axis',(0.866025403784438,0.,0.5));
#21004=DIRECTION('center_axis',(-0.5,0.,-0.866025403784438));
#21005=DIRECTION('ref_axis',(0.866025403784438,0.,-0.500000000000001));
#21006=DIRECTION('center_axis',(0.5,0.,-0.866025403784438));
#21007=DIRECTION('ref_axis',(0.866025403784438,0.,0.5));
#21008=DIRECTION('center_axis',(0.5,0.,0.866025403784438));
#21009=DIRECTION('ref_axis',(-0.866025403784438,0.,0.5));
#21010=DIRECTION('',(0.,-1.,0.));
#21011=DIRECTION('',(-0.866025403784438,0.,0.5));
#21012=DIRECTION('',(-0.866025403784438,0.,0.5));
#21013=DIRECTION('',(-0.866025403784438,0.,0.5));
#21014=DIRECTION('',(0.,-1.,0.));
#21015=DIRECTION('',(-0.866025403784438,0.,0.5));
#21016=DIRECTION('',(0.,-1.,0.));
#21017=DIRECTION('center_axis',(0.,1.,0.));
#21018=DIRECTION('ref_axis',(0.,0.,1.));
#21019=DIRECTION('center_axis',(0.,-1.,0.));
#21020=DIRECTION('ref_axis',(1.,0.,0.));
#21021=DIRECTION('center_axis',(0.,-1.,0.));
#21022=DIRECTION('ref_axis',(1.,0.,0.));
#21023=DIRECTION('',(0.,-1.,0.));
#21024=DIRECTION('center_axis',(0.,1.,0.));
#21025=DIRECTION('ref_axis',(1.,0.,0.));
#21026=DIRECTION('center_axis',(0.,1.,0.));
#21027=DIRECTION('ref_axis',(0.,0.,1.));
#21028=DIRECTION('',(0.866025403784439,0.,0.5));
#21029=DIRECTION('center_axis',(0.,-1.,0.));
#21030=DIRECTION('ref_axis',(1.,0.,0.));
#21031=DIRECTION('center_axis',(0.,1.,0.));
#21032=DIRECTION('ref_axis',(0.,0.,1.));
#21033=DIRECTION('',(0.866025403784439,0.,-0.5));
#21034=DIRECTION('center_axis',(0.,-1.,0.));
#21035=DIRECTION('ref_axis',(1.,0.,0.));
#21036=DIRECTION('center_axis',(0.,1.,0.));
#21037=DIRECTION('ref_axis',(0.,0.,1.));
#21038=DIRECTION('',(3.39346356420629E-16,0.,1.));
#21039=DIRECTION('center_axis',(0.,-1.,0.));
#21040=DIRECTION('ref_axis',(1.,0.,0.));
#21041=DIRECTION('center_axis',(0.,1.,0.));
#21042=DIRECTION('ref_axis',(0.,0.,1.));
#21043=DIRECTION('',(0.,0.,-1.));
#21044=DIRECTION('center_axis',(0.,-1.,0.));
#21045=DIRECTION('ref_axis',(1.,0.,0.));
#21046=DIRECTION('center_axis',(0.,-1.,0.));
#21047=DIRECTION('ref_axis',(1.,0.,0.));
#21048=DIRECTION('center_axis',(0.,1.,0.));
#21049=DIRECTION('ref_axis',(0.,0.,1.));
#21050=DIRECTION('center_axis',(0.,-1.,0.));
#21051=DIRECTION('ref_axis',(1.,0.,0.));
#21052=DIRECTION('center_axis',(0.,1.,0.));
#21053=DIRECTION('ref_axis',(0.,0.,1.));
#21054=DIRECTION('',(-0.866025403784438,0.,-0.5));
#21055=DIRECTION('center_axis',(0.,-1.,0.));
#21056=DIRECTION('ref_axis',(1.,0.,0.));
#21057=DIRECTION('center_axis',(0.,-1.,0.));
#21058=DIRECTION('ref_axis',(1.,0.,0.));
#21059=DIRECTION('center_axis',(0.,-1.,0.));
#21060=DIRECTION('ref_axis',(1.,0.,0.));
#21061=DIRECTION('',(0.,1.,0.));
#21062=DIRECTION('center_axis',(0.,1.,0.));
#21063=DIRECTION('ref_axis',(1.,0.,0.));
#21064=DIRECTION('center_axis',(0.,1.,0.));
#21065=DIRECTION('ref_axis',(1.,0.,0.));
#21066=DIRECTION('center_axis',(0.,1.,0.));
#21067=DIRECTION('ref_axis',(1.,0.,0.));
#21068=DIRECTION('center_axis',(0.,1.,0.));
#21069=DIRECTION('ref_axis',(1.,0.,0.));
#21070=DIRECTION('center_axis',(0.,1.,0.));
#21071=DIRECTION('ref_axis',(1.,0.,0.));
#21072=DIRECTION('center_axis',(0.,1.,0.));
#21073=DIRECTION('ref_axis',(1.,0.,0.));
#21074=DIRECTION('center_axis',(0.,1.,0.));
#21075=DIRECTION('ref_axis',(1.,0.,0.));
#21076=DIRECTION('center_axis',(0.,-1.,0.));
#21077=DIRECTION('ref_axis',(1.,0.,0.));
#21078=DIRECTION('',(-0.707106781186549,0.707106781186546,-8.65956056235495E-17));
#21079=DIRECTION('center_axis',(0.,-1.,0.));
#21080=DIRECTION('ref_axis',(0.,0.,-1.));
#21081=DIRECTION('center_axis',(0.,-1.,0.));
#21082=DIRECTION('ref_axis',(0.,0.,-1.));
#21083=DIRECTION('',(0.866025403784439,0.,0.5));
#21084=DIRECTION('',(3.39346356420629E-16,0.,1.));
#21085=DIRECTION('center_axis',(0.,-1.,0.));
#21086=DIRECTION('ref_axis',(0.,0.,-1.));
#21087=DIRECTION('',(3.39346356420629E-16,0.,1.));
#21088=DIRECTION('center_axis',(0.,-1.,0.));
#21089=DIRECTION('ref_axis',(0.,0.,-1.));
#21090=DIRECTION('',(0.866025403784439,0.,-0.5));
#21091=DIRECTION('',(0.866025403784439,0.,0.5));
#21092=DIRECTION('center_axis',(0.,-1.,0.));
#21093=DIRECTION('ref_axis',(0.,0.,-1.));
#21094=DIRECTION('',(-0.866025403784438,0.,-0.5));
#21095=DIRECTION('center_axis',(0.,-1.,0.));
#21096=DIRECTION('ref_axis',(0.,0.,-1.));
#21097=DIRECTION('',(0.,0.,-1.));
#21098=DIRECTION('',(0.866025403784439,0.,-0.5));
#21099=DIRECTION('center_axis',(0.,1.,0.));
#21100=DIRECTION('ref_axis',(1.,0.,0.));
#21101=DIRECTION('',(0.866025403784439,0.,0.5));
#21102=DIRECTION('',(0.866025403784439,0.,-0.5));
#21103=DIRECTION('',(0.,0.,-1.));
#21104=DIRECTION('',(-0.866025403784438,0.,-0.5));
#21105=DIRECTION('',(3.39346356420629E-16,0.,1.));
#21106=DIRECTION('center_axis',(0.,-1.,0.));
#21107=DIRECTION('ref_axis',(1.,0.,0.));
#21108=DIRECTION('center_axis',(-0.5,0.,-0.866025403784439));
#21109=DIRECTION('ref_axis',(0.866025403784439,0.,-0.5));
#21110=DIRECTION('',(0.,-1.,0.));
#21111=DIRECTION('',(0.,-1.,0.));
#21112=DIRECTION('center_axis',(-1.,0.,0.));
#21113=DIRECTION('ref_axis',(0.,0.,-1.));
#21114=DIRECTION('',(0.,0.,-1.));
#21115=DIRECTION('',(0.,-1.,0.));
#21116=DIRECTION('center_axis',(-0.5,0.,0.866025403784438));
#21117=DIRECTION('ref_axis',(-0.866025403784438,0.,-0.5));
#21118=DIRECTION('',(-0.866025403784438,0.,-0.5));
#21119=DIRECTION('center_axis',(1.,0.,-3.39346356420629E-16));
#21120=DIRECTION('ref_axis',(3.39346356420629E-16,0.,1.));
#21121=DIRECTION('',(0.,-1.,0.));
#21122=DIRECTION('center_axis',(0.5,0.,-0.866025403784439));
#21123=DIRECTION('ref_axis',(0.866025403784439,0.,0.5));
#21124=DIRECTION('center_axis',(0.,-1.,0.));
#21125=DIRECTION('ref_axis',(0.,0.,-1.));
#21126=DIRECTION('center_axis',(0.,1.,0.));
#21127=DIRECTION('ref_axis',(0.,0.,1.));
#21128=DIRECTION('center_axis',(0.,-1.,0.));
#21129=DIRECTION('ref_axis',(1.,0.,0.));
#21130=DIRECTION('center_axis',(0.,-1.,0.));
#21131=DIRECTION('ref_axis',(1.,0.,0.));
#21132=DIRECTION('center_axis',(0.,-1.,0.));
#21133=DIRECTION('ref_axis',(1.,0.,0.));
#21134=DIRECTION('',(0.514495755427528,0.857492925712543,6.30075580059222E-17));
#21135=DIRECTION('center_axis',(0.,-1.,0.));
#21136=DIRECTION('ref_axis',(1.,0.,0.));
#21137=DIRECTION('',(0.,1.,0.));
#36071=CARTESIAN_POINT('',(0.,0.,0.));
#36072=CARTESIAN_POINT('Origin',(-27.,-76.,44.));
#36073=CARTESIAN_POINT('',(-45.,-77.5,44.));
#36074=CARTESIAN_POINT('',(-42.,-80.5,44.));
#36075=CARTESIAN_POINT('Origin',(-42.,-77.5,44.));
#36076=CARTESIAN_POINT('',(-45.,-74.5,44.));
#36077=CARTESIAN_POINT('',(-45.,-74.5,44.));
#36078=CARTESIAN_POINT('',(-42.,-71.5,44.));
#36079=CARTESIAN_POINT('Origin',(-42.,-74.5,44.));
#36080=CARTESIAN_POINT('',(-12.,-71.5,44.));
#36081=CARTESIAN_POINT('',(-12.,-71.5,44.));
#36082=CARTESIAN_POINT('',(-9.,-74.5,44.));
#36083=CARTESIAN_POINT('Origin',(-12.,-74.5,44.));
#36084=CARTESIAN_POINT('',(-9.,-77.5,44.));
#36085=CARTESIAN_POINT('',(-9.,-77.5,44.));
#36086=CARTESIAN_POINT('',(-12.,-80.5,44.));
#36087=CARTESIAN_POINT('Origin',(-12.,-77.5,44.));
#36088=CARTESIAN_POINT('',(-42.,-80.5,44.));
#36089=CARTESIAN_POINT('',(-17.,-76.,44.));
#36090=CARTESIAN_POINT('Origin',(-14.,-76.,44.));
#36091=CARTESIAN_POINT('Origin',(-45.,-74.5,44.));
#36092=CARTESIAN_POINT('',(-45.,-77.5,47.));
#36093=CARTESIAN_POINT('',(-45.,-77.5,44.));
#36094=CARTESIAN_POINT('',(-45.,-74.5,47.));
#36095=CARTESIAN_POINT('',(-45.,-74.5,47.));
#36096=CARTESIAN_POINT('',(-45.,-74.5,44.));
#36097=CARTESIAN_POINT('Origin',(-42.,-74.5,44.));
#36098=CARTESIAN_POINT('',(-42.,-71.5,47.));
#36099=CARTESIAN_POINT('Origin',(-42.,-74.5,47.));
#36100=CARTESIAN_POINT('',(-42.,-71.5,44.));
#36101=CARTESIAN_POINT('Origin',(-12.,-71.5,44.));
#36102=CARTESIAN_POINT('',(-12.,-71.5,47.));
#36103=CARTESIAN_POINT('',(-12.,-71.5,47.));
#36104=CARTESIAN_POINT('',(-12.,-71.5,44.));
#36105=CARTESIAN_POINT('Origin',(-12.,-74.5,44.));
#36106=CARTESIAN_POINT('',(-9.,-74.5,47.));
#36107=CARTESIAN_POINT('Origin',(-12.,-74.5,47.));
#36108=CARTESIAN_POINT('',(-9.,-74.5,44.));
#36109=CARTESIAN_POINT('Origin',(-9.,-77.5,44.));
#36110=CARTESIAN_POINT('',(-8.99999999999999,-77.5,47.));
#36111=CARTESIAN_POINT('',(-9.,-77.5,47.));
#36112=CARTESIAN_POINT('',(-9.,-77.5,44.));
#36113=CARTESIAN_POINT('Origin',(-12.,-77.5,44.));
#36114=CARTESIAN_POINT('',(-12.,-80.5,47.));
#36115=CARTESIAN_POINT('Origin',(-12.,-77.5,47.));
#36116=CARTESIAN_POINT('',(-12.,-80.5,44.));
#36117=CARTESIAN_POINT('Origin',(-42.,-80.5,44.));
#36118=CARTESIAN_POINT('',(-42.,-80.5,47.));
#36119=CARTESIAN_POINT('',(-42.,-80.5,47.));
#36120=CARTESIAN_POINT('',(-42.,-80.5,44.));
#36121=CARTESIAN_POINT('Origin',(-42.,-77.5,44.));
#36122=CARTESIAN_POINT('Origin',(-42.,-77.5,47.));
#36123=CARTESIAN_POINT('Origin',(-27.,-76.,47.));
#36124=CARTESIAN_POINT('Origin',(-14.,-76.,38.));
#36125=CARTESIAN_POINT('',(-17.,-76.,38.0829037686548));
#36126=CARTESIAN_POINT('',(-17.,-76.,38.));
#36127=CARTESIAN_POINT('',(-14.,-79.,39.8149545762236));
#36128=CARTESIAN_POINT('Origin',(-14.,-76.,39.8149545762236));
#36129=CARTESIAN_POINT('',(-14.,-73.,39.8149545762236));
#36130=CARTESIAN_POINT('Origin',(-14.,-76.,39.8149545762236));
#36131=CARTESIAN_POINT('Origin',(-14.,-76.,39.8149545762236));
#36132=CARTESIAN_POINT('Origin',(-5.5,-72.,34.9074772881118));
#36133=CARTESIAN_POINT('',(-14.,-95.,39.8149545762236));
#36134=CARTESIAN_POINT('',(-14.,-72.,39.8149545762236));
#36135=CARTESIAN_POINT('',(-12.3117376914899,-95.,38.8402358779426));
#36136=CARTESIAN_POINT('',(-5.5,-95.,34.9074772881118));
#36137=CARTESIAN_POINT('',(-7.1882623085101,-95.,35.8821959863928));
#36138=CARTESIAN_POINT('',(-5.5,-95.,34.9074772881118));
#36139=CARTESIAN_POINT('',(-5.5,-95.,34.9074772881118));
#36140=CARTESIAN_POINT('',(-5.5,-95.,34.9074772881118));
#36141=CARTESIAN_POINT('',(-5.5,-72.,34.9074772881118));
#36142=CARTESIAN_POINT('',(-5.5,-72.,34.9074772881118));
#36143=CARTESIAN_POINT('',(-14.,-72.,39.8149545762236));
#36144=CARTESIAN_POINT('',(-5.5,-72.,34.9074772881118));
#36145=CARTESIAN_POINT('',(-14.,-72.,39.8149545762236));
#36146=CARTESIAN_POINT('Origin',(-8.4,-96.,30.));
#36147=CARTESIAN_POINT('',(-19.6,-96.,30.));
#36148=CARTESIAN_POINT('Origin',(-14.,-96.,30.));
#36149=CARTESIAN_POINT('Origin',(-14.,-100.55,30.));
#36150=CARTESIAN_POINT('',(-19.6,-105.,30.));
#36151=CARTESIAN_POINT('',(-19.6,-100.55,30.));
#36152=CARTESIAN_POINT('Origin',(-14.,-105.,30.));
#36153=CARTESIAN_POINT('Origin',(-5.,-95.,30.));
#36154=CARTESIAN_POINT('',(-12.3117376914899,-95.,21.1597641220574));
#36155=CARTESIAN_POINT('',(-7.18826230851011,-95.,24.1178040136072));
#36156=CARTESIAN_POINT('',(-14.,-95.,20.1850454237764));
#36157=CARTESIAN_POINT('Origin',(-14.,-95.,30.));
#36158=CARTESIAN_POINT('Origin',(-5.,-95.,30.));
#36159=CARTESIAN_POINT('',(-20.8117376914899,-95.,24.1178040136072));
#36160=CARTESIAN_POINT('',(-15.6882623085101,-95.,21.1597641220574));
#36161=CARTESIAN_POINT('',(-22.5,-95.,25.0925227118882));
#36162=CARTESIAN_POINT('Origin',(-14.,-95.,30.));
#36163=CARTESIAN_POINT('Origin',(-5.,-95.,30.));
#36164=CARTESIAN_POINT('',(-5.5,-95.,27.0419601084502));
#36165=CARTESIAN_POINT('',(-5.5,-95.,32.9580398915498));
#36166=CARTESIAN_POINT('',(-5.5,-95.,25.0925227118882));
#36167=CARTESIAN_POINT('Origin',(-14.,-95.,30.));
#36168=CARTESIAN_POINT('Origin',(-5.,-95.,30.));
#36169=CARTESIAN_POINT('',(-22.5,-95.,32.9580398915498));
#36170=CARTESIAN_POINT('',(-22.5,-95.,27.0419601084502));
#36171=CARTESIAN_POINT('',(-22.5,-95.,34.9074772881118));
#36172=CARTESIAN_POINT('',(-23.,-95.,30.));
#36173=CARTESIAN_POINT('Origin',(-14.,-95.,30.));
#36174=CARTESIAN_POINT('Origin',(-14.,-95.,30.));
#36175=CARTESIAN_POINT('Origin',(-5.,-95.,30.));
#36176=CARTESIAN_POINT('Origin',(-14.,-95.,30.));
#36177=CARTESIAN_POINT('Origin',(-5.,-95.,30.));
#36178=CARTESIAN_POINT('',(-15.6882623085101,-95.,38.8402358779426));
#36179=CARTESIAN_POINT('',(-20.8117376914899,-95.,35.8821959863928));
#36180=CARTESIAN_POINT('',(-14.,-95.,39.8149545762236));
#36181=CARTESIAN_POINT('Origin',(-14.,-95.,30.));
#36182=CARTESIAN_POINT('Origin',(-14.,-99.5,30.));
#36183=CARTESIAN_POINT('',(-23.,-104.,30.));
#36184=CARTESIAN_POINT('Origin',(-14.,-104.,30.));
#36185=CARTESIAN_POINT('',(-23.,-99.5,30.));
#36186=CARTESIAN_POINT('Origin',(-14.,-95.,30.));
#36187=CARTESIAN_POINT('Origin',(-14.,-95.,30.));
#36188=CARTESIAN_POINT('Origin',(-14.,-95.,30.));
#36189=CARTESIAN_POINT('Origin',(-14.,-95.,30.));
#36190=CARTESIAN_POINT('Origin',(-14.,-95.,30.));
#36191=CARTESIAN_POINT('Origin',(-14.,-95.,30.));
#36192=CARTESIAN_POINT('Origin',(-14.,-104.5,30.));
#36193=CARTESIAN_POINT('',(-22.,-105.,30.));
#36194=CARTESIAN_POINT('Origin',(-14.,-105.,30.));
#36195=CARTESIAN_POINT('',(-22.5,-104.5,30.));
#36196=CARTESIAN_POINT('Origin',(-14.,-105.,30.));
#36197=CARTESIAN_POINT('Origin',(-14.,-95.,30.));
#36198=CARTESIAN_POINT('',(-5.5,-95.,25.0925227118882));
#36199=CARTESIAN_POINT('',(-14.,-95.,20.1850454237764));
#36200=CARTESIAN_POINT('',(-5.5,-95.,25.0925227118882));
#36201=CARTESIAN_POINT('Origin',(-14.,-95.,30.));
#36202=CARTESIAN_POINT('',(-5.5,-95.,25.0925227118882));
#36203=CARTESIAN_POINT('Origin',(-14.,-95.,30.));
#36204=CARTESIAN_POINT('',(-14.,-95.,20.1850454237764));
#36205=CARTESIAN_POINT('',(-22.5,-95.,25.0925227118882));
#36206=CARTESIAN_POINT('',(-14.,-95.,20.1850454237764));
#36207=CARTESIAN_POINT('Origin',(-14.,-95.,30.));
#36208=CARTESIAN_POINT('',(-14.,-95.,39.8149545762236));
#36209=CARTESIAN_POINT('Origin',(-14.,-95.,30.));
#36210=CARTESIAN_POINT('',(-22.5,-95.,25.0925227118882));
#36211=CARTESIAN_POINT('',(-22.5,-95.,34.9074772881118));
#36212=CARTESIAN_POINT('',(-22.5,-95.,25.0925227118882));
#36213=CARTESIAN_POINT('Origin',(-14.,-72.,30.));
#36214=CARTESIAN_POINT('',(-14.,-72.,20.1850454237764));
#36215=CARTESIAN_POINT('',(-5.5,-72.,25.0925227118882));
#36216=CARTESIAN_POINT('',(-14.,-72.,20.1850454237764));
#36217=CARTESIAN_POINT('',(-22.5,-72.,25.0925227118882));
#36218=CARTESIAN_POINT('',(-22.5,-72.,25.0925227118882));
#36219=CARTESIAN_POINT('',(-22.5,-72.,34.9074772881118));
#36220=CARTESIAN_POINT('',(-22.5,-72.,34.9074772881118));
#36221=CARTESIAN_POINT('',(-14.,-72.,39.8149545762236));
#36222=CARTESIAN_POINT('',(-5.5,-72.,25.0925227118882));
#36223=CARTESIAN_POINT('',(-20.8,-72.,30.));
#36224=CARTESIAN_POINT('Origin',(-14.,-72.,30.));
#36225=CARTESIAN_POINT('Origin',(-22.5,-72.,25.0925227118882));
#36226=CARTESIAN_POINT('',(-14.,-72.,20.1850454237764));
#36227=CARTESIAN_POINT('',(-22.5,-72.,25.0925227118882));
#36228=CARTESIAN_POINT('Origin',(-22.5,-72.,34.9074772881118));
#36229=CARTESIAN_POINT('',(-22.5,-95.,34.9074772881118));
#36230=CARTESIAN_POINT('',(-22.5,-95.,34.9074772881118));
#36231=CARTESIAN_POINT('',(-22.5,-72.,34.9074772881118));
#36232=CARTESIAN_POINT('Origin',(-14.,-72.,39.8149545762236));
#36233=CARTESIAN_POINT('',(-14.,-95.,39.8149545762236));
#36234=CARTESIAN_POINT('Origin',(-5.5,-72.,25.0925227118882));
#36235=CARTESIAN_POINT('',(-5.5,-72.,25.0925227118882));
#36236=CARTESIAN_POINT('Origin',(-14.,-72.,20.1850454237764));
#36237=CARTESIAN_POINT('Origin',(-14.,-95.,30.));
#36238=CARTESIAN_POINT('Origin',(-7.5,-60.5,30.));
#36239=CARTESIAN_POINT('',(-20.5,-60.5,30.));
#36240=CARTESIAN_POINT('Origin',(-14.,-60.5,30.));
#36241=CARTESIAN_POINT('Origin',(-14.,-60.75,30.));
#36242=CARTESIAN_POINT('',(-20.8,-61.,30.));
#36243=CARTESIAN_POINT('Origin',(-14.,-61.,30.));
#36244=CARTESIAN_POINT('',(-20.65,-60.75,30.));
#36245=CARTESIAN_POINT('Origin',(-14.,-66.5,30.));
#36246=CARTESIAN_POINT('',(-20.8,-66.5,30.));
#56608=UNCERTAINTY_MEASURE_WITH_UNIT(LENGTH_MEASURE(0.01),#56640,
'DISTANCE_ACCURACY_VALUE',
'Maximum model space distance between geometric entities at asserted c
onnectivities');
#56617=UNCERTAINTY_MEASURE_WITH_UNIT(LENGTH_MEASURE(0.01),#56640,
'DISTANCE_ACCURACY_VALUE',
'Maximum model space distance between geometric entities at asserted c
onnectivities');
#56630=(
GEOMETRIC_REPRESENTATION_CONTEXT(3)
GLOBAL_UNCERTAINTY_ASSIGNED_CONTEXT((#56608))
GLOBAL_UNIT_ASSIGNED_CONTEXT((#56640,#56642,#56643))
REPRESENTATION_CONTEXT('','3D')
);
#56639=(
GEOMETRIC_REPRESENTATION_CONTEXT(3)
GLOBAL_UNCERTAINTY_ASSIGNED_CONTEXT((#56617))
GLOBAL_UNIT_ASSIGNED_CONTEXT((#56640,#56642,#56643))
REPRESENTATION_CONTEXT('','3D')
);
#56640=(
LENGTH_UNIT()
NAMED_UNIT(*)
SI_UNIT(.MILLI.,.METRE.)
);
#56642=(
NAMED_UNIT(*)
PLANE_ANGLE_UNIT()
SI_UNIT($,.RADIAN.)
);
#56643=(
NAMED_UNIT(*)
SI_UNIT($,.STERADIAN.)
SOLID_ANGLE_UNIT()
);
#56656=SHAPE_DEFINITION_REPRESENTATION(#56677,#56756);
#56677=PRODUCT_DEFINITION_SHAPE('',$,#56778);
#56756=SHAPE_REPRESENTATION('',(#18066),#56630);
#56765=PRODUCT_DEFINITION_CONTEXT('part definition',#56830,'design');
#56778=PRODUCT_DEFINITION('2026-10-26-00-02-57-738',
'19_Air_Inlet_Ball_Valve_1-4',#56799,#56765);
#56799=PRODUCT_DEFINITION_FORMATION('',$,#56844);
#56830=APPLICATION_CONTEXT(
'Core Data for Automotive Mechanical Design Process');
#56831=PRODUCT_CONTEXT('part definition',#56830,'mechanical');
#56844=PRODUCT('2026-10-26-00-02-57-738','19_Air_Inlet_Ball_Valve_1-4',
$,(#56831));
#56923=COLOUR_RGB('Off White',0.89,0.88,0.83);
#56924=FILL_AREA_STYLE_COLOUR('',#56923);
#56925=FILL_AREA_STYLE('',(#56924));
#56926=SURFACE_STYLE_FILL_AREA(#56925);
#56927=SURFACE_SIDE_STYLE('',(#56926));
#56928=SURFACE_STYLE_USAGE(.BOTH.,#56927);
#56929=PRESENTATION_STYLE_ASSIGNMENT((#56928));
ENDSEC;
END-ISO-10303-21;
